ISO-10303-21;
HEADER;
/* Generated by software containing ST-Developer
 * from STEP Tools, Inc. (www.steptools.com) 
 */

FILE_DESCRIPTION(
/* description */ ('Dual-rail gantry carriage'),
/* implementation_level */ '2;1');

FILE_NAME(
/* name */ 'Cap Screw - M5x20.step',
/* time_stamp */ '2026-10-27T10:49:15-07:00',
/* author */ (''),
/* organization */ (''),
/* preprocessor_version */ 'ST-DEVELOPER v20.2',
/* originating_system */ 'Autodesk Translation Framework v15.17.0.0',
/* authorisation */ '');

FILE_SCHEMA (('AUTOMOTIVE_DESIGN { 1 0 10303 214 3 1 1 }'));
ENDSEC;

DATA;
#10=MECHANICAL_DESIGN_GEOMETRIC_PRESENTATION_REPRESENTATION('',(#611),#12804);
#495=ORIENTED_CLOSED_SHELL('',*,#7392,.F.);
#506=CONICAL_SURFACE('',#8347,0.4,0.785398163397448);
#507=CONICAL_SURFACE('',#8351,0.41,0.785398163397448);
#508=CONICAL_SURFACE('',#8355,0.26,0.463647609000806);
#509=CONICAL_SURFACE('',#8359,0.225,0.785398163397448);
#520=BREP_WITH_VOIDS('Body1',#7391,(#495));
#549=SHAPE_REPRESENTATION_RELATIONSHIP('SRR','None',#13029,#580);
#580=ADVANCED_BREP_SHAPE_REPRESENTATION('',(#520),#12799);
#611=STYLED_ITEM('',(#13254),#520);
#757=FACE_BOUND('',#1887,.T.);
#1011=PLANE('',#8345);
#1012=PLANE('',#8353);
#1013=PLANE('',#8361);
#1014=PLANE('',#8362);
#1015=PLANE('',#8363);
#1016=PLANE('',#8364);
#1017=PLANE('',#8365);
#1018=PLANE('',#8366);
#1019=PLANE('',#8367);
#1020=PLANE('',#8368);
#1021=PLANE('',#8369);
#1378=FACE_OUTER_BOUND('',#1882,.T.);
#1379=FACE_OUTER_BOUND('',#1883,.T.);
#1380=FACE_OUTER_BOUND('',#1884,.T.);
#1381=FACE_OUTER_BOUND('',#1885,.T.);
#1382=FACE_OUTER_BOUND('',#1886,.T.);
#1383=FACE_OUTER_BOUND('',#1888,.T.);
#1384=FACE_OUTER_BOUND('',#1889,.T.);
#1385=FACE_OUTER_BOUND('',#1890,.T.);
#1386=FACE_OUTER_BOUND('',#1891,.T.);
#1387=FACE_OUTER_BOUND('',#1892,.T.);
#1388=FACE_OUTER_BOUND('',#1893,.T.);
#1389=FACE_OUTER_BOUND('',#1894,.T.);
#1390=FACE_OUTER_BOUND('',#1895,.T.);
#1391=FACE_OUTER_BOUND('',#1896,.T.);
#1392=FACE_OUTER_BOUND('',#1897,.T.);
#1393=FACE_OUTER_BOUND('',#1898,.T.);
#1394=FACE_OUTER_BOUND('',#1899,.T.);
#1882=EDGE_LOOP('',(#6673));
#1883=EDGE_LOOP('',(#6674,#6675,#6676,#6677));
#1884=EDGE_LOOP('',(#6678,#6679,#6680,#6681));
#1885=EDGE_LOOP('',(#6682,#6683,#6684,#6685));
#1886=EDGE_LOOP('',(#6686));
#1887=EDGE_LOOP('',(#6687));
#1888=EDGE_LOOP('',(#6688,#6689,#6690,#6691));
#1889=EDGE_LOOP('',(#6692,#6693,#6694,#6695));
#1890=EDGE_LOOP('',(#6696,#6697,#6698,#6699));
#1891=EDGE_LOOP('',(#6700));
#1892=EDGE_LOOP('',(#6701,#6702,#6703,#6704));
#1893=EDGE_LOOP('',(#6705,#6706,#6707,#6708));
#1894=EDGE_LOOP('',(#6709,#6710,#6711,#6712));
#1895=EDGE_LOOP('',(#6713,#6714,#6715,#6716));
#1896=EDGE_LOOP('',(#6717,#6718,#6719,#6720));
#1897=EDGE_LOOP('',(#6721,#6722,#6723,#6724));
#1898=EDGE_LOOP('',(#6725,#6726,#6727,#6728,#6729,#6730));
#1899=EDGE_LOOP('',(#6731,#6732,#6733,#6734,#6735,#6736));
#2581=LINE('',#12453,#3290);
#2582=LINE('',#12457,#3291);
#2583=LINE('',#12461,#3292);
#2584=LINE('',#12468,#3293);
#2585=LINE('',#12472,#3294);
#2586=LINE('',#12476,#3295);
#2587=LINE('',#12481,#3296);
#2588=LINE('',#12483,#3297);
#2589=LINE('',#12485,#3298);
#2590=LINE('',#12486,#3299);
#2591=LINE('',#12489,#3300);
#2592=LINE('',#12491,#3301);
#2593=LINE('',#12492,#3302);
#2594=LINE('',#12495,#3303);
#2595=LINE('',#12497,#3304);
#2596=LINE('',#12498,#3305);
#2597=LINE('',#12501,#3306);
#2598=LINE('',#12503,#3307);
#2599=LINE('',#12504,#3308);
#2600=LINE('',#12507,#3309);
#2601=LINE('',#12509,#3310);
#2602=LINE('',#12510,#3311);
#2603=LINE('',#12512,#3312);
#2604=LINE('',#12513,#3313);
#3290=VECTOR('',#10336,0.4);
#3291=VECTOR('',#10341,0.425);
#3292=VECTOR('',#10346,0.41);
#3293=VECTOR('',#10355,0.26);
#3294=VECTOR('',#10360,0.25);
#3295=VECTOR('',#10365,0.225);
#3296=VECTOR('',#10370,1.);
#3297=VECTOR('',#10371,1.);
#3298=VECTOR('',#10372,1.);
#3299=VECTOR('',#10373,1.);
#3300=VECTOR('',#10376,1.);
#3301=VECTOR('',#10377,1.);
#3302=VECTOR('',#10378,1.);
#3303=VECTOR('',#10381,1.);
#3304=VECTOR('',#10382,1.);
#3305=VECTOR('',#10383,1.);
#3306=VECTOR('',#10386,1.);
#3307=VECTOR('',#10387,1.);
#3308=VECTOR('',#10388,1.);
#3309=VECTOR('',#10391,1.);
#3310=VECTOR('',#10392,1.);
#3311=VECTOR('',#10393,1.);
#3312=VECTOR('',#10396,1.);
#3313=VECTOR('',#10397,1.);
#3534=CIRCLE('',#8346,0.375);
#3535=CIRCLE('',#8348,0.425);
#3536=CIRCLE('',#8350,0.425);
#3537=CIRCLE('',#8352,0.395);
#3538=CIRCLE('',#8354,0.27);
#3539=CIRCLE('',#8356,0.24505);
#3540=CIRCLE('',#8358,0.24505);
#3541=CIRCLE('',#8360,0.2);
#4088=VERTEX_POINT('',#12448);
#4089=VERTEX_POINT('',#12451);
#4090=VERTEX_POINT('',#12455);
#4091=VERTEX_POINT('',#12459);
#4092=VERTEX_POINT('',#12463);
#4093=VERTEX_POINT('',#12466);
#4094=VERTEX_POINT('',#12470);
#4095=VERTEX_POINT('',#12474);
#4096=VERTEX_POINT('',#12479);
#4097=VERTEX_POINT('',#12480);
#4098=VERTEX_POINT('',#12482);
#4099=VERTEX_POINT('',#12484);
#4100=VERTEX_POINT('',#12488);
#4101=VERTEX_POINT('',#12490);
#4102=VERTEX_POINT('',#12494);
#4103=VERTEX_POINT('',#12496);
#4104=VERTEX_POINT('',#12500);
#4105=VERTEX_POINT('',#12502);
#4106=VERTEX_POINT('',#12506);
#4107=VERTEX_POINT('',#12508);
#4959=EDGE_CURVE('',#4088,#4088,#3534,.T.);
#4960=EDGE_CURVE('',#4089,#4089,#3535,.T.);
#4961=EDGE_CURVE('',#4089,#4088,#2581,.T.);
#4962=EDGE_CURVE('',#4090,#4090,#3536,.T.);
#4963=EDGE_CURVE('',#4090,#4089,#2582,.T.);
#4964=EDGE_CURVE('',#4091,#4091,#3537,.T.);
#4965=EDGE_CURVE('',#4091,#4090,#2583,.T.);
#4966=EDGE_CURVE('',#4092,#4092,#3538,.T.);
#4967=EDGE_CURVE('',#4093,#4093,#3539,.F.);
#4968=EDGE_CURVE('',#4093,#4092,#2584,.T.);
#4969=EDGE_CURVE('',#4094,#4094,#3540,.F.);
#4970=EDGE_CURVE('',#4094,#4093,#2585,.T.);
#4971=EDGE_CURVE('',#4095,#4095,#3541,.T.);
#4972=EDGE_CURVE('',#4095,#4094,#2586,.T.);
#4973=EDGE_CURVE('',#4096,#4097,#2587,.T.);
#4974=EDGE_CURVE('',#4097,#4098,#2588,.T.);
#4975=EDGE_CURVE('',#4098,#4099,#2589,.T.);
#4976=EDGE_CURVE('',#4096,#4099,#2590,.T.);
#4977=EDGE_CURVE('',#4097,#4100,#2591,.T.);
#4978=EDGE_CURVE('',#4100,#4101,#2592,.T.);
#4979=EDGE_CURVE('',#4101,#4098,#2593,.T.);
#4980=EDGE_CURVE('',#4100,#4102,#2594,.T.);
#4981=EDGE_CURVE('',#4102,#4103,#2595,.T.);
#4982=EDGE_CURVE('',#4103,#4101,#2596,.T.);
#4983=EDGE_CURVE('',#4102,#4104,#2597,.T.);
#4984=EDGE_CURVE('',#4104,#4105,#2598,.T.);
#4985=EDGE_CURVE('',#4105,#4103,#2599,.T.);
#4986=EDGE_CURVE('',#4104,#4106,#2600,.T.);
#4987=EDGE_CURVE('',#4106,#4107,#2601,.T.);
#4988=EDGE_CURVE('',#4107,#4105,#2602,.T.);
#4989=EDGE_CURVE('',#4106,#4096,#2603,.T.);
#4990=EDGE_CURVE('',#4099,#4107,#2604,.T.);
#6673=ORIENTED_EDGE('',*,*,#4959,.F.);
#6674=ORIENTED_EDGE('',*,*,#4960,.F.);
#6675=ORIENTED_EDGE('',*,*,#4961,.T.);
#6676=ORIENTED_EDGE('',*,*,#4959,.T.);
#6677=ORIENTED_EDGE('',*,*,#4961,.F.);
#6678=ORIENTED_EDGE('',*,*,#4962,.F.);
#6679=ORIENTED_EDGE('',*,*,#4963,.T.);
#6680=ORIENTED_EDGE('',*,*,#4960,.T.);
#6681=ORIENTED_EDGE('',*,*,#4963,.F.);
#6682=ORIENTED_EDGE('',*,*,#4964,.F.);
#6683=ORIENTED_EDGE('',*,*,#4965,.T.);
#6684=ORIENTED_EDGE('',*,*,#4962,.T.);
#6685=ORIENTED_EDGE('',*,*,#4965,.F.);
#6686=ORIENTED_EDGE('',*,*,#4964,.T.);
#6687=ORIENTED_EDGE('',*,*,#4966,.F.);
#6688=ORIENTED_EDGE('',*,*,#4967,.F.);
#6689=ORIENTED_EDGE('',*,*,#4968,.T.);
#6690=ORIENTED_EDGE('',*,*,#4966,.T.);
#6691=ORIENTED_EDGE('',*,*,#4968,.F.);
#6692=ORIENTED_EDGE('',*,*,#4969,.F.);
#6693=ORIENTED_EDGE('',*,*,#4970,.T.);
#6694=ORIENTED_EDGE('',*,*,#4967,.T.);
#6695=ORIENTED_EDGE('',*,*,#4970,.F.);
#6696=ORIENTED_EDGE('',*,*,#4971,.F.);
#6697=ORIENTED_EDGE('',*,*,#4972,.T.);
#6698=ORIENTED_EDGE('',*,*,#4969,.T.);
#6699=ORIENTED_EDGE('',*,*,#4972,.F.);
#6700=ORIENTED_EDGE('',*,*,#4971,.T.);
#6701=ORIENTED_EDGE('',*,*,#4973,.T.);
#6702=ORIENTED_EDGE('',*,*,#4974,.T.);
#6703=ORIENTED_EDGE('',*,*,#4975,.T.);
#6704=ORIENTED_EDGE('',*,*,#4976,.F.);
#6705=ORIENTED_EDGE('',*,*,#4977,.T.);
#6706=ORIENTED_EDGE('',*,*,#4978,.T.);
#6707=ORIENTED_EDGE('',*,*,#4979,.T.);
#6708=ORIENTED_EDGE('',*,*,#4974,.F.);
#6709=ORIENTED_EDGE('',*,*,#4980,.T.);
#6710=ORIENTED_EDGE('',*,*,#4981,.T.);
#6711=ORIENTED_EDGE('',*,*,#4982,.T.);
#6712=ORIENTED_EDGE('',*,*,#4978,.F.);
#6713=ORIENTED_EDGE('',*,*,#4983,.T.);
#6714=ORIENTED_EDGE('',*,*,#4984,.T.);
#6715=ORIENTED_EDGE('',*,*,#4985,.T.);
#6716=ORIENTED_EDGE('',*,*,#4981,.F.);
#6717=ORIENTED_EDGE('',*,*,#4986,.T.);
#6718=ORIENTED_EDGE('',*,*,#4987,.T.);
#6719=ORIENTED_EDGE('',*,*,#4988,.T.);
#6720=ORIENTED_EDGE('',*,*,#4984,.F.);
#6721=ORIENTED_EDGE('',*,*,#4989,.T.);
#6722=ORIENTED_EDGE('',*,*,#4976,.T.);
#6723=ORIENTED_EDGE('',*,*,#4990,.T.);
#6724=ORIENTED_EDGE('',*,*,#4987,.F.);
#6725=ORIENTED_EDGE('',*,*,#4989,.F.);
#6726=ORIENTED_EDGE('',*,*,#4986,.F.);
#6727=ORIENTED_EDGE('',*,*,#4983,.F.);
#6728=ORIENTED_EDGE('',*,*,#4980,.F.);
#6729=ORIENTED_EDGE('',*,*,#4977,.F.);
#6730=ORIENTED_EDGE('',*,*,#4973,.F.);
#6731=ORIENTED_EDGE('',*,*,#4990,.F.);
#6732=ORIENTED_EDGE('',*,*,#4975,.F.);
#6733=ORIENTED_EDGE('',*,*,#4979,.F.);
#6734=ORIENTED_EDGE('',*,*,#4982,.F.);
#6735=ORIENTED_EDGE('',*,*,#4985,.F.);
#6736=ORIENTED_EDGE('',*,*,#4988,.F.);
#6964=CYLINDRICAL_SURFACE('',#8349,0.425);
#6965=CYLINDRICAL_SURFACE('',#8357,0.24505);
#7304=ADVANCED_FACE('',(#1378),#1011,.T.);
#7305=ADVANCED_FACE('',(#1379),#506,.T.);
#7306=ADVANCED_FACE('',(#1380),#6964,.T.);
#7307=ADVANCED_FACE('',(#1381),#507,.T.);
#7308=ADVANCED_FACE('',(#1382,#757),#1012,.T.);
#7309=ADVANCED_FACE('',(#1383),#508,.T.);
#7310=ADVANCED_FACE('',(#1384),#6965,.T.);
#7311=ADVANCED_FACE('',(#1385),#509,.T.);
#7312=ADVANCED_FACE('',(#1386),#1013,.T.);
#7313=ADVANCED_FACE('',(#1387),#1014,.F.);
#7314=ADVANCED_FACE('',(#1388),#1015,.F.);
#7315=ADVANCED_FACE('',(#1389),#1016,.F.);
#7316=ADVANCED_FACE('',(#1390),#1017,.F.);
#7317=ADVANCED_FACE('',(#1391),#1018,.F.);
#7318=ADVANCED_FACE('',(#1392),#1019,.F.);
#7319=ADVANCED_FACE('',(#1393),#1020,.F.);
#7320=ADVANCED_FACE('',(#1394),#1021,.F.);
#7391=CLOSED_SHELL('',(#7304,#7305,#7306,#7307,#7308,#7309,#7310,#7311,
#7312));
#7392=CLOSED_SHELL('',(#7313,#7314,#7315,#7316,#7317,#7318,#7319,#7320));
#8344=AXIS2_PLACEMENT_3D('',#12446,#10326,#10327);
#8345=AXIS2_PLACEMENT_3D('',#12447,#10328,#10329);
#8346=AXIS2_PLACEMENT_3D('',#12449,#10330,#10331);
#8347=AXIS2_PLACEMENT_3D('',#12450,#10332,#10333);
#8348=AXIS2_PLACEMENT_3D('',#12452,#10334,#10335);
#8349=AXIS2_PLACEMENT_3D('',#12454,#10337,#10338);
#8350=AXIS2_PLACEMENT_3D('',#12456,#10339,#10340);
#8351=AXIS2_PLACEMENT_3D('',#12458,#10342,#10343);
#8352=AXIS2_PLACEMENT_3D('',#12460,#10344,#10345);
#8353=AXIS2_PLACEMENT_3D('',#12462,#10347,#10348);
#8354=AXIS2_PLACEMENT_3D('',#12464,#10349,#10350);
#8355=AXIS2_PLACEMENT_3D('',#12465,#10351,#10352);
#8356=AXIS2_PLACEMENT_3D('',#12467,#10353,#10354);
#8357=AXIS2_PLACEMENT_3D('',#12469,#10356,#10357);
#8358=AXIS2_PLACEMENT_3D('',#12471,#10358,#10359);
#8359=AXIS2_PLACEMENT_3D('',#12473,#10361,#10362);
#8360=AXIS2_PLACEMENT_3D('',#12475,#10363,#10364);
#8361=AXIS2_PLACEMENT_3D('',#12477,#10366,#10367);
#8362=AXIS2_PLACEMENT_3D('',#12478,#10368,#10369);
#8363=AXIS2_PLACEMENT_3D('',#12487,#10374,#10375);
#8364=AXIS2_PLACEMENT_3D('',#12493,#10379,#10380);
#8365=AXIS2_PLACEMENT_3D('',#12499,#10384,#10385);
#8366=AXIS2_PLACEMENT_3D('',#12505,#10389,#10390);
#8367=AXIS2_PLACEMENT_3D('',#12511,#10394,#10395);
#8368=AXIS2_PLACEMENT_3D('',#12514,#10398,#10399);
#8369=AXIS2_PLACEMENT_3D('',#12515,#10400,#10401);
#10326=DIRECTION('axis',(0.,0.,1.));
#10327=DIRECTION('refdir',(1.,0.,0.));
#10328=DIRECTION('center_axis',(0.,1.,0.));
#10329=DIRECTION('ref_axis',(0.,0.,1.));
#10330=DIRECTION('center_axis',(0.,-1.,0.));
#10331=DIRECTION('ref_axis',(1.,0.,0.));
#10332=DIRECTION('center_axis',(0.,-1.,0.));
#10333=DIRECTION('ref_axis',(1.,0.,0.));
#10334=DIRECTION('center_axis',(0.,-1.,0.));
#10335=DIRECTION('ref_axis',(1.,0.,0.));
#10336=DIRECTION('',(0.707106781186548,0.707106781186547,8.65956056235493E-17));
#10337=DIRECTION('center_axis',(0.,-1.,0.));
#10338=DIRECTION('ref_axis',(1.,0.,0.));
#10339=DIRECTION('center_axis',(0.,-1.,0.));
#10340=DIRECTION('ref_axis',(1.,0.,0.));
#10341=DIRECTION('',(0.,1.,0.));
#10342=DIRECTION('center_axis',(0.,1.,0.));
#10343=DIRECTION('ref_axis',(1.,0.,0.));
#10344=DIRECTION('center_axis',(0.,-1.,0.));
#10345=DIRECTION('ref_axis',(1.,0.,0.));
#10346=DIRECTION('',(-0.707106781186547,0.707106781186548,-8.65956056235493E-17));
#10347=DIRECTION('center_axis',(0.,-1.,0.));
#10348=DIRECTION('ref_axis',(0.,0.,-1.));
#10349=DIRECTION('center_axis',(0.,-1.,0.));
#10350=DIRECTION('ref_axis',(1.,0.,0.));
#10351=DIRECTION('center_axis',(0.,1.,0.));
#10352=DIRECTION('ref_axis',(1.,0.,0.));
#10353=DIRECTION('center_axis',(0.,1.,0.));
#10354=DIRECTION('ref_axis',(1.,0.,0.));
#10355=DIRECTION('',(-0.447213595499958,0.894427190999916,-5.47678698264203E-17));
#10356=DIRECTION('center_axis',(0.,-1.,0.));
#10357=DIRECTION('ref_axis',(1.,0.,0.));
#10358=DIRECTION('center_axis',(0.,1.,0.));
#10359=DIRECTION('ref_axis',(1.,0.,0.));
#10360=DIRECTION('',(0.,1.,0.));
#10361=DIRECTION('center_axis',(0.,1.,0.));
#10362=DIRECTION('ref_axis',(1.,0.,0.));
#10363=DIRECTION('center_axis',(0.,-1.,0.));
#10364=DIRECTION('ref_axis',(1.,0.,0.));
#10365=DIRECTION('',(-0.707106781186547,0.707106781186548,-8.65956056235493E-17));
#10366=DIRECTION('center_axis',(0.,-1.,0.));
#10367=DIRECTION('ref_axis',(0.,0.,-1.));
#10368=DIRECTION('center_axis',(0.866025403784439,0.,-0.5));
#10369=DIRECTION('ref_axis',(0.5,0.,0.866025403784439));
#10370=DIRECTION('',(-0.5,0.,-0.866025403784439));
#10371=DIRECTION('',(0.,-1.,0.));
#10372=DIRECTION('',(0.5,0.,0.866025403784439));
#10373=DIRECTION('',(0.,-1.,0.));
#10374=DIRECTION('center_axis',(1.20185167898973E-16,0.,-1.));
#10375=DIRECTION('ref_axis',(1.,0.,1.20185167898973E-16));
#10376=DIRECTION('',(-1.,0.,-1.20185167898973E-16));
#10377=DIRECTION('',(0.,-1.,0.));
#10378=DIRECTION('',(1.,0.,1.20185167898973E-16));
#10379=DIRECTION('center_axis',(-0.866025403784439,0.,-0.5));
#10380=DIRECTION('ref_axis',(0.5,0.,-0.866025403784439));
#10381=DIRECTION('',(-0.5,0.,0.866025403784439));
#10382=DIRECTION('',(0.,-1.,0.));
#10383=DIRECTION('',(0.5,0.,-0.866025403784439));
#10384=DIRECTION('center_axis',(-0.866025403784439,0.,0.5));
#10385=DIRECTION('ref_axis',(-0.5,0.,-0.866025403784439));
#10386=DIRECTION('',(0.5,0.,0.866025403784439));
#10387=DIRECTION('',(0.,-1.,0.));
#10388=DIRECTION('',(-0.5,0.,-0.866025403784439));
#10389=DIRECTION('center_axis',(-2.40370335797945E-16,0.,1.));
#10390=DIRECTION('ref_axis',(-1.,0.,-2.40370335797945E-16));
#10391=DIRECTION('',(1.,0.,2.40370335797945E-16));
#10392=DIRECTION('',(0.,-1.,0.));
#10393=DIRECTION('',(-1.,0.,-2.40370335797945E-16));
#10394=DIRECTION('center_axis',(0.866025403784439,0.,0.5));
#10395=DIRECTION('ref_axis',(-0.5,0.,0.866025403784439));
#10396=DIRECTION('',(0.5,0.,-0.866025403784439));
#10397=DIRECTION('',(-0.5,0.,0.866025403784439));
#10398=DIRECTION('center_axis',(0.,1.,0.));
#10399=DIRECTION('ref_axis',(1.,0.,0.));
#10400=DIRECTION('center_axis',(0.,-1.,0.));
#10401=DIRECTION('ref_axis',(0.,0.,-1.));
#12446=CARTESIAN_POINT('',(0.,0.,0.));
#12447=CARTESIAN_POINT('Origin',(0.375,0.5,0.));
#12448=CARTESIAN_POINT('',(-0.375,0.5,-4.59242549680257E-17));
#12449=CARTESIAN_POINT('Origin',(0.,0.5,0.));
#12450=CARTESIAN_POINT('Origin',(0.,0.475,0.));
#12451=CARTESIAN_POINT('',(-0.425,0.45,-5.20474889637625E-17));
#12452=CARTESIAN_POINT('Origin',(0.,0.45,0.));
#12453=CARTESIAN_POINT('',(-0.4,0.475,-4.89858719658941E-17));
#12454=CARTESIAN_POINT('Origin',(0.,0.24,0.));
#12455=CARTESIAN_POINT('',(-0.425,0.0299999999999998,-5.20474889637625E-17));
#12456=CARTESIAN_POINT('Origin',(0.,0.0299999999999998,0.));
#12457=CARTESIAN_POINT('',(-0.425,0.24,-5.20474889637625E-17));
#12458=CARTESIAN_POINT('Origin',(0.,0.0150000000000001,0.));
#12459=CARTESIAN_POINT('',(-0.395,4.85722573273506E-17,-4.83735485663204E-17));
#12460=CARTESIAN_POINT('Origin',(0.,0.,0.));
#12461=CARTESIAN_POINT('',(-0.41,0.0150000000000001,-5.02105187650415E-17));
#12462=CARTESIAN_POINT('Origin',(0.27,0.,0.));
#12463=CARTESIAN_POINT('',(-0.27,0.,-3.30654635769785E-17));
#12464=CARTESIAN_POINT('Origin',(0.,0.,0.));
#12465=CARTESIAN_POINT('Origin',(0.,-0.02,0.));
#12466=CARTESIAN_POINT('',(-0.24505,-0.0498999999999999,3.00099698131059E-17));
#12467=CARTESIAN_POINT('Origin',(0.,-0.0498999999999999,0.));
#12468=CARTESIAN_POINT('',(-0.26,-0.02,-3.18408167778312E-17));
#12469=CARTESIAN_POINT('Origin',(0.,-0.995,0.));
#12470=CARTESIAN_POINT('',(-0.24505,-1.95495,3.00099698131059E-17));
#12471=CARTESIAN_POINT('Origin',(0.,-1.95495,0.));
#12472=CARTESIAN_POINT('',(-0.24505,-0.995,-3.00099698131059E-17));
#12473=CARTESIAN_POINT('Origin',(0.,-1.975,0.));
#12474=CARTESIAN_POINT('',(-0.2,-2.,-2.44929359829471E-17));
#12475=CARTESIAN_POINT('Origin',(0.,-2.,0.));
#12476=CARTESIAN_POINT('',(-0.225,-1.975,-2.75545529808154E-17));
#12477=CARTESIAN_POINT('Origin',(0.,-2.,0.));
#12478=CARTESIAN_POINT('Origin',(0.115470053837925,-0.5,-0.2));
#12479=CARTESIAN_POINT('',(0.23094010767585,-0.5,0.));
#12480=CARTESIAN_POINT('',(0.115470053837925,-0.5,-0.2));
#12481=CARTESIAN_POINT('',(0.23094010767585,-0.5,0.));
#12482=CARTESIAN_POINT('',(0.115470053837925,-0.8,-0.2));
#12483=CARTESIAN_POINT('',(0.115470053837925,-0.5,-0.2));
#12484=CARTESIAN_POINT('',(0.23094010767585,-0.8,0.));
#12485=CARTESIAN_POINT('',(0.23094010767585,-0.8,0.));
#12486=CARTESIAN_POINT('',(0.23094010767585,-0.5,0.));
#12487=CARTESIAN_POINT('Origin',(-0.115470053837925,-0.5,-0.2));
#12488=CARTESIAN_POINT('',(-0.115470053837925,-0.5,-0.2));
#12489=CARTESIAN_POINT('',(0.115470053837925,-0.5,-0.2));
#12490=CARTESIAN_POINT('',(-0.115470053837925,-0.8,-0.2));
#12491=CARTESIAN_POINT('',(-0.115470053837925,-0.5,-0.2));
#12492=CARTESIAN_POINT('',(0.115470053837925,-0.8,-0.2));
#12493=CARTESIAN_POINT('Origin',(-0.23094010767585,-0.5,-2.77555756156289E-17));
#12494=CARTESIAN_POINT('',(-0.23094010767585,-0.5,-2.82820063659975E-17));
#12495=CARTESIAN_POINT('',(-0.115470053837925,-0.5,-0.2));
#12496=CARTESIAN_POINT('',(-0.23094010767585,-0.8,-2.77555756156289E-17));
#12497=CARTESIAN_POINT('',(-0.23094010767585,-0.5,-2.82820063659975E-17));
#12498=CARTESIAN_POINT('',(-0.115470053837925,-0.8,-0.2));
#12499=CARTESIAN_POINT('Origin',(-0.115470053837925,-0.5,0.2));
#12500=CARTESIAN_POINT('',(-0.115470053837925,-0.5,0.2));
#12501=CARTESIAN_POINT('',(-0.23094010767585,-0.5,-2.82820063659975E-17));
#12502=CARTESIAN_POINT('',(-0.115470053837925,-0.8,0.2));
#12503=CARTESIAN_POINT('',(-0.115470053837925,-0.5,0.2));
#12504=CARTESIAN_POINT('',(-0.23094010767585,-0.8,-2.82820063659975E-17));
#12505=CARTESIAN_POINT('Origin',(0.115470053837925,-0.5,0.2));
#12506=CARTESIAN_POINT('',(0.115470053837925,-0.5,0.2));
#12507=CARTESIAN_POINT('',(-0.115470053837925,-0.5,0.2));
#12508=CARTESIAN_POINT('',(0.115470053837925,-0.8,0.2));
#12509=CARTESIAN_POINT('',(0.115470053837925,-0.5,0.2));
#12510=CARTESIAN_POINT('',(-0.115470053837925,-0.8,0.2));
#12511=CARTESIAN_POINT('Origin',(0.23094010767585,-0.5,0.));
#12512=CARTESIAN_POINT('',(0.115470053837925,-0.5,0.2));
#12513=CARTESIAN_POINT('',(0.115470053837925,-0.8,0.2));
#12514=CARTESIAN_POINT('Origin',(0.,-0.5,0.));
#12515=CARTESIAN_POINT('Origin',(0.,-0.8,0.));
#12763=UNCERTAINTY_MEASURE_WITH_UNIT(LENGTH_MEASURE(0.001),#12805,
'DISTANCE_ACCURACY_VALUE',
'Maximum model space distance between geometric entities at asserted c
onnectivities');
#12768=UNCERTAINTY_MEASURE_WITH_UNIT(LENGTH_MEASURE(0.001),#12805,
'DISTANCE_ACCURACY_VALUE',
'Maximum model space distance between geometric entities at asserted c
onnectivities');
#12799=(
GEOMETRIC_REPRESENTATION_CONTEXT(3)
GLOBAL_UNCERTAINTY_ASSIGNED_CONTEXT((#12763))
GLOBAL_UNIT_ASSIGNED_CONTEXT((#12805,#12807,#12808))
REPRESENTATION_CONTEXT('','3D')
);
#12804=(
GEOMETRIC_REPRESENTATION_CONTEXT(3)
GLOBAL_UNCERTAINTY_ASSIGNED_CONTEXT((#12768))
GLOBAL_UNIT_ASSIGNED_CONTEXT((#12805,#12807,#12808))
REPRESENTATION_CONTEXT('','3D')
);
#12805=(
LENGTH_UNIT()
NAMED_UNIT(*)
SI_UNIT(.CENTI.,.METRE.)
);
#12807=(
NAMED_UNIT(*)
PLANE_ANGLE_UNIT()
SI_UNIT($,.RADIAN.)
);
#12808=(
NAMED_UNIT(*)
SI_UNIT($,.STERADIAN.)
SOLID_ANGLE_UNIT()
);
#12839=SHAPE_DEFINITION_REPRESENTATION(#12947,#13029);
#12947=PRODUCT_DEFINITION_SHAPE('',$,#13065);
#13029=SHAPE_REPRESENTATION('',(#8344),#12799);
#13034=PRODUCT_DEFINITION_CONTEXT('part definition',#13141,'design');
#13065=PRODUCT_DEFINITION('Cap Screw - M5x20','Cap Screw - M5x20',#13100,
#13034);
#13100=PRODUCT_DEFINITION_FORMATION('',$,#13173);
#13141=APPLICATION_CONTEXT(
'Core Data for Automotive Mechanical Design Process');
#13142=PRODUCT_CONTEXT('part definition',#13141,'mechanical');
#13173=PRODUCT('Cap Screw - M5x20','Cap Screw - M5x20',
'Cap Screw - M5x20',(#13142));
#13248=COLOUR_RGB('Black',0.12,0.14,0.17);
#13249=FILL_AREA_STYLE_COLOUR('',#13248);
#13250=FILL_AREA_STYLE('',(#13249));
#13251=SURFACE_STYLE_FILL_AREA(#13250);
#13252=SURFACE_SIDE_STYLE('',(#13251));
#13253=SURFACE_STYLE_USAGE(.BOTH.,#13252);
#13254=PRESENTATION_STYLE_ASSIGNMENT((#13253));
ENDSEC;
END-ISO-10303-21;
